ISO-10303-21;
HEADER;
/* Generated by software containing ST-Developer
 * from STEP Tools, Inc. (www.steptools.com) 
 */

FILE_DESCRIPTION(
/* description */ ('Turntable on roller ring'),
/* implementation_level */ '2;1');

FILE_NAME(
/* name */ 'M6x18 mounting screw.step',
/* time_stamp */ '2026-10-28T03:23:59-07:00',
/* author */ (''),
/* organization */ (''),
/* preprocessor_version */ 'ST-DEVELOPER v20.2',
/* originating_system */ 'Autodesk Translation Framework v15.17.0.0',
/* authorisation */ '');

FILE_SCHEMA (('AUTOMOTIVE_DESIGN { 1 0 10303 214 3 1 1 }'));
ENDSEC;

DATA;
#10=MECHANICAL_DESIGN_GEOMETRIC_PRESENTATION_REPRESENTATION('',(#620),#16281);
#476=CONICAL_SURFACE('',#9219,0.475,0.785398163397449);
#477=CONICAL_SURFACE('',#9223,0.485,0.785398163397448);
#478=CONICAL_SURFACE('',#9227,0.31,0.463647609000806);
#499=ORIENTED_CLOSED_SHELL('',*,#8361,.F.);
#503=BREP_WITH_VOIDS('Body1',#8362,(#499));
#510=SHAPE_REPRESENTATION_RELATIONSHIP('SRR','None',#16524,#565);
#565=ADVANCED_BREP_SHAPE_REPRESENTATION('',(#503),#16218);
#620=STYLED_ITEM('',(#16939),#503);
#823=FACE_BOUND('',#1901,.T.);
#1010=PLANE('',#9207);
#1011=PLANE('',#9208);
#1012=PLANE('',#9209);
#1013=PLANE('',#9210);
#1014=PLANE('',#9211);
#1015=PLANE('',#9212);
#1016=PLANE('',#9213);
#1017=PLANE('',#9214);
#1018=PLANE('',#9215);
#1019=PLANE('',#9217);
#1020=PLANE('',#9225);
#1316=FACE_OUTER_BOUND('',#1887,.T.);
#1317=FACE_OUTER_BOUND('',#1888,.T.);
#1318=FACE_OUTER_BOUND('',#1889,.T.);
#1319=FACE_OUTER_BOUND('',#1890,.T.);
#1320=FACE_OUTER_BOUND('',#1891,.T.);
#1321=FACE_OUTER_BOUND('',#1892,.T.);
#1322=FACE_OUTER_BOUND('',#1893,.T.);
#1323=FACE_OUTER_BOUND('',#1894,.T.);
#1324=FACE_OUTER_BOUND('',#1895,.T.);
#1325=FACE_OUTER_BOUND('',#1896,.T.);
#1326=FACE_OUTER_BOUND('',#1897,.T.);
#1327=FACE_OUTER_BOUND('',#1898,.T.);
#1328=FACE_OUTER_BOUND('',#1899,.T.);
#1329=FACE_OUTER_BOUND('',#1900,.T.);
#1330=FACE_OUTER_BOUND('',#1902,.T.);
#1331=FACE_OUTER_BOUND('',#1903,.T.);
#1887=EDGE_LOOP('',(#5959,#5960,#5961,#5962));
#1888=EDGE_LOOP('',(#5963,#5964,#5965,#5966));
#1889=EDGE_LOOP('',(#5967,#5968,#5969,#5970));
#1890=EDGE_LOOP('',(#5971,#5972,#5973,#5974));
#1891=EDGE_LOOP('',(#5975,#5976,#5977,#5978));
#1892=EDGE_LOOP('',(#5979,#5980,#5981,#5982));
#1893=EDGE_LOOP('',(#5983,#5984,#5985,#5986,#5987,#5988));
#1894=EDGE_LOOP('',(#5989,#5990,#5991,#5992,#5993,#5994));
#1895=EDGE_LOOP('',(#5995));
#1896=EDGE_LOOP('',(#5996));
#1897=EDGE_LOOP('',(#5997,#5998,#5999,#6000));
#1898=EDGE_LOOP('',(#6001,#6002,#6003,#6004));
#1899=EDGE_LOOP('',(#6005,#6006,#6007,#6008));
#1900=EDGE_LOOP('',(#6009));
#1901=EDGE_LOOP('',(#6010));
#1902=EDGE_LOOP('',(#6011,#6012,#6013,#6014));
#1903=EDGE_LOOP('',(#6015,#6016,#6017,#6018));
#2555=LINE('',#13334,#3038);
#2556=LINE('',#13336,#3039);
#2557=LINE('',#13338,#3040);
#2558=LINE('',#13339,#3041);
#2559=LINE('',#13342,#3042);
#2560=LINE('',#13344,#3043);
#2561=LINE('',#13345,#3044);
#2562=LINE('',#13348,#3045);
#2563=LINE('',#13350,#3046);
#2564=LINE('',#13351,#3047);
#2565=LINE('',#13354,#3048);
#2566=LINE('',#13356,#3049);
#2567=LINE('',#13357,#3050);
#2568=LINE('',#13360,#3051);
#2569=LINE('',#13362,#3052);
#2570=LINE('',#13363,#3053);
#2571=LINE('',#13365,#3054);
#2572=LINE('',#13366,#3055);
#2573=LINE('',#13378,#3056);
#2574=LINE('',#13382,#3057);
#2575=LINE('',#13386,#3058);
#2576=LINE('',#13393,#3059);
#2577=LINE('',#13395,#3060);
#3038=VECTOR('',#10598,1.);
#3039=VECTOR('',#10599,1.);
#3040=VECTOR('',#10600,1.);
#3041=VECTOR('',#10601,1.);
#3042=VECTOR('',#10604,1.);
#3043=VECTOR('',#10605,1.);
#3044=VECTOR('',#10606,1.);
#3045=VECTOR('',#10609,1.);
#3046=VECTOR('',#10610,1.);
#3047=VECTOR('',#10611,1.);
#3048=VECTOR('',#10614,1.);
#3049=VECTOR('',#10615,1.);
#3050=VECTOR('',#10616,1.);
#3051=VECTOR('',#10619,1.);
#3052=VECTOR('',#10620,1.);
#3053=VECTOR('',#10621,1.);
#3054=VECTOR('',#10624,1.);
#3055=VECTOR('',#10625,1.);
#3056=VECTOR('',#10642,0.475);
#3057=VECTOR('',#10647,0.5);
#3058=VECTOR('',#10652,0.485);
#3059=VECTOR('',#10661,0.31);
#3060=VECTOR('',#10664,0.3);
#3554=CIRCLE('',#9216,0.2942);
#3555=CIRCLE('',#9218,0.45);
#3556=CIRCLE('',#9220,0.5);
#3557=CIRCLE('',#9222,0.5);
#3558=CIRCLE('',#9224,0.47);
#3559=CIRCLE('',#9226,0.32);
#3560=CIRCLE('',#9228,0.2942);
#4048=VERTEX_POINT('',#13332);
#4049=VERTEX_POINT('',#13333);
#4050=VERTEX_POINT('',#13335);
#4051=VERTEX_POINT('',#13337);
#4052=VERTEX_POINT('',#13341);
#4053=VERTEX_POINT('',#13343);
#4054=VERTEX_POINT('',#13347);
#4055=VERTEX_POINT('',#13349);
#4056=VERTEX_POINT('',#13353);
#4057=VERTEX_POINT('',#13355);
#4058=VERTEX_POINT('',#13359);
#4059=VERTEX_POINT('',#13361);
#4060=VERTEX_POINT('',#13370);
#4061=VERTEX_POINT('',#13373);
#4062=VERTEX_POINT('',#13376);
#4063=VERTEX_POINT('',#13380);
#4064=VERTEX_POINT('',#13384);
#4065=VERTEX_POINT('',#13388);
#4066=VERTEX_POINT('',#13391);
#4790=EDGE_CURVE('',#4048,#4049,#2555,.T.);
#4791=EDGE_CURVE('',#4049,#4050,#2556,.T.);
#4792=EDGE_CURVE('',#4050,#4051,#2557,.T.);
#4793=EDGE_CURVE('',#4048,#4051,#2558,.T.);
#4794=EDGE_CURVE('',#4049,#4052,#2559,.T.);
#4795=EDGE_CURVE('',#4052,#4053,#2560,.T.);
#4796=EDGE_CURVE('',#4053,#4050,#2561,.T.);
#4797=EDGE_CURVE('',#4052,#4054,#2562,.T.);
#4798=EDGE_CURVE('',#4054,#4055,#2563,.T.);
#4799=EDGE_CURVE('',#4055,#4053,#2564,.T.);
#4800=EDGE_CURVE('',#4054,#4056,#2565,.T.);
#4801=EDGE_CURVE('',#4056,#4057,#2566,.T.);
#4802=EDGE_CURVE('',#4057,#4055,#2567,.T.);
#4803=EDGE_CURVE('',#4056,#4058,#2568,.T.);
#4804=EDGE_CURVE('',#4058,#4059,#2569,.T.);
#4805=EDGE_CURVE('',#4059,#4057,#2570,.T.);
#4806=EDGE_CURVE('',#4058,#4048,#2571,.T.);
#4807=EDGE_CURVE('',#4051,#4059,#2572,.T.);
#4808=EDGE_CURVE('',#4060,#4060,#3554,.T.);
#4809=EDGE_CURVE('',#4061,#4061,#3555,.T.);
#4810=EDGE_CURVE('',#4062,#4062,#3556,.T.);
#4811=EDGE_CURVE('',#4062,#4061,#2573,.T.);
#4812=EDGE_CURVE('',#4063,#4063,#3557,.T.);
#4813=EDGE_CURVE('',#4063,#4062,#2574,.T.);
#4814=EDGE_CURVE('',#4064,#4064,#3558,.T.);
#4815=EDGE_CURVE('',#4064,#4063,#2575,.T.);
#4816=EDGE_CURVE('',#4065,#4065,#3559,.T.);
#4817=EDGE_CURVE('',#4066,#4066,#3560,.F.);
#4818=EDGE_CURVE('',#4066,#4065,#2576,.T.);
#4819=EDGE_CURVE('',#4060,#4066,#2577,.T.);
#5959=ORIENTED_EDGE('',*,*,#4790,.T.);
#5960=ORIENTED_EDGE('',*,*,#4791,.T.);
#5961=ORIENTED_EDGE('',*,*,#4792,.T.);
#5962=ORIENTED_EDGE('',*,*,#4793,.F.);
#5963=ORIENTED_EDGE('',*,*,#4794,.T.);
#5964=ORIENTED_EDGE('',*,*,#4795,.T.);
#5965=ORIENTED_EDGE('',*,*,#4796,.T.);
#5966=ORIENTED_EDGE('',*,*,#4791,.F.);
#5967=ORIENTED_EDGE('',*,*,#4797,.T.);
#5968=ORIENTED_EDGE('',*,*,#4798,.T.);
#5969=ORIENTED_EDGE('',*,*,#4799,.T.);
#5970=ORIENTED_EDGE('',*,*,#4795,.F.);
#5971=ORIENTED_EDGE('',*,*,#4800,.T.);
#5972=ORIENTED_EDGE('',*,*,#4801,.T.);
#5973=ORIENTED_EDGE('',*,*,#4802,.T.);
#5974=ORIENTED_EDGE('',*,*,#4798,.F.);
#5975=ORIENTED_EDGE('',*,*,#4803,.T.);
#5976=ORIENTED_EDGE('',*,*,#4804,.T.);
#5977=ORIENTED_EDGE('',*,*,#4805,.T.);
#5978=ORIENTED_EDGE('',*,*,#4801,.F.);
#5979=ORIENTED_EDGE('',*,*,#4806,.T.);
#5980=ORIENTED_EDGE('',*,*,#4793,.T.);
#5981=ORIENTED_EDGE('',*,*,#4807,.T.);
#5982=ORIENTED_EDGE('',*,*,#4804,.F.);
#5983=ORIENTED_EDGE('',*,*,#4806,.F.);
#5984=ORIENTED_EDGE('',*,*,#4803,.F.);
#5985=ORIENTED_EDGE('',*,*,#4800,.F.);
#5986=ORIENTED_EDGE('',*,*,#4797,.F.);
#5987=ORIENTED_EDGE('',*,*,#4794,.F.);
#5988=ORIENTED_EDGE('',*,*,#4790,.F.);
#5989=ORIENTED_EDGE('',*,*,#4807,.F.);
#5990=ORIENTED_EDGE('',*,*,#4792,.F.);
#5991=ORIENTED_EDGE('',*,*,#4796,.F.);
#5992=ORIENTED_EDGE('',*,*,#4799,.F.);
#5993=ORIENTED_EDGE('',*,*,#4802,.F.);
#5994=ORIENTED_EDGE('',*,*,#4805,.F.);
#5995=ORIENTED_EDGE('',*,*,#4808,.F.);
#5996=ORIENTED_EDGE('',*,*,#4809,.F.);
#5997=ORIENTED_EDGE('',*,*,#4810,.F.);
#5998=ORIENTED_EDGE('',*,*,#4811,.T.);
#5999=ORIENTED_EDGE('',*,*,#4809,.T.);
#6000=ORIENTED_EDGE('',*,*,#4811,.F.);
#6001=ORIENTED_EDGE('',*,*,#4812,.F.);
#6002=ORIENTED_EDGE('',*,*,#4813,.T.);
#6003=ORIENTED_EDGE('',*,*,#4810,.T.);
#6004=ORIENTED_EDGE('',*,*,#4813,.F.);
#6005=ORIENTED_EDGE('',*,*,#4814,.F.);
#6006=ORIENTED_EDGE('',*,*,#4815,.T.);
#6007=ORIENTED_EDGE('',*,*,#4812,.T.);
#6008=ORIENTED_EDGE('',*,*,#4815,.F.);
#6009=ORIENTED_EDGE('',*,*,#4814,.T.);
#6010=ORIENTED_EDGE('',*,*,#4816,.F.);
#6011=ORIENTED_EDGE('',*,*,#4817,.F.);
#6012=ORIENTED_EDGE('',*,*,#4818,.T.);
#6013=ORIENTED_EDGE('',*,*,#4816,.T.);
#6014=ORIENTED_EDGE('',*,*,#4818,.F.);
#6015=ORIENTED_EDGE('',*,*,#4808,.T.);
#6016=ORIENTED_EDGE('',*,*,#4819,.T.);
#6017=ORIENTED_EDGE('',*,*,#4817,.T.);
#6018=ORIENTED_EDGE('',*,*,#4819,.F.);
#7715=CYLINDRICAL_SURFACE('',#9221,0.5);
#7716=CYLINDRICAL_SURFACE('',#9229,0.2942);
#7919=ADVANCED_FACE('',(#1316),#1010,.F.);
#7920=ADVANCED_FACE('',(#1317),#1011,.F.);
#7921=ADVANCED_FACE('',(#1318),#1012,.F.);
#7922=ADVANCED_FACE('',(#1319),#1013,.F.);
#7923=ADVANCED_FACE('',(#1320),#1014,.F.);
#7924=ADVANCED_FACE('',(#1321),#1015,.F.);
#7925=ADVANCED_FACE('',(#1322),#1016,.F.);
#7926=ADVANCED_FACE('',(#1323),#1017,.F.);
#7927=ADVANCED_FACE('',(#1324),#1018,.F.);
#7928=ADVANCED_FACE('',(#1325),#1019,.T.);
#7929=ADVANCED_FACE('',(#1326),#476,.T.);
#7930=ADVANCED_FACE('',(#1327),#7715,.T.);
#7931=ADVANCED_FACE('',(#1328),#477,.T.);
#7932=ADVANCED_FACE('',(#1329,#823),#1020,.T.);
#7933=ADVANCED_FACE('',(#1330),#478,.T.);
#7934=ADVANCED_FACE('',(#1331),#7716,.T.);
#8361=CLOSED_SHELL('',(#7919,#7920,#7921,#7922,#7923,#7924,#7925,#7926));
#8362=CLOSED_SHELL('',(#7927,#7928,#7929,#7930,#7931,#7932,#7933,#7934));
#9206=AXIS2_PLACEMENT_3D('',#13330,#10594,#10595);
#9207=AXIS2_PLACEMENT_3D('',#13331,#10596,#10597);
#9208=AXIS2_PLACEMENT_3D('',#13340,#10602,#10603);
#9209=AXIS2_PLACEMENT_3D('',#13346,#10607,#10608);
#9210=AXIS2_PLACEMENT_3D('',#13352,#10612,#10613);
#9211=AXIS2_PLACEMENT_3D('',#13358,#10617,#10618);
#9212=AXIS2_PLACEMENT_3D('',#13364,#10622,#10623);
#9213=AXIS2_PLACEMENT_3D('',#13367,#10626,#10627);
#9214=AXIS2_PLACEMENT_3D('',#13368,#10628,#10629);
#9215=AXIS2_PLACEMENT_3D('',#13369,#10630,#10631);
#9216=AXIS2_PLACEMENT_3D('',#13371,#10632,#10633);
#9217=AXIS2_PLACEMENT_3D('',#13372,#10634,#10635);
#9218=AXIS2_PLACEMENT_3D('',#13374,#10636,#10637);
#9219=AXIS2_PLACEMENT_3D('',#13375,#10638,#10639);
#9220=AXIS2_PLACEMENT_3D('',#13377,#10640,#10641);
#9221=AXIS2_PLACEMENT_3D('',#13379,#10643,#10644);
#9222=AXIS2_PLACEMENT_3D('',#13381,#10645,#10646);
#9223=AXIS2_PLACEMENT_3D('',#13383,#10648,#10649);
#9224=AXIS2_PLACEMENT_3D('',#13385,#10650,#10651);
#9225=AXIS2_PLACEMENT_3D('',#13387,#10653,#10654);
#9226=AXIS2_PLACEMENT_3D('',#13389,#10655,#10656);
#9227=AXIS2_PLACEMENT_3D('',#13390,#10657,#10658);
#9228=AXIS2_PLACEMENT_3D('',#13392,#10659,#10660);
#9229=AXIS2_PLACEMENT_3D('',#13394,#10662,#10663);
#10594=DIRECTION('axis',(0.,0.,1.));
#10595=DIRECTION('refdir',(1.,0.,0.));
#10596=DIRECTION('center_axis',(0.866025403784439,0.,-0.5));
#10597=DIRECTION('ref_axis',(0.5,0.,0.866025403784439));
#10598=DIRECTION('',(-0.5,0.,-0.866025403784439));
#10599=DIRECTION('',(0.,-1.,0.));
#10600=DIRECTION('',(0.5,0.,0.866025403784439));
#10601=DIRECTION('',(0.,-1.,0.));
#10602=DIRECTION('center_axis',(1.92296268638356E-16,0.,-1.));
#10603=DIRECTION('ref_axis',(1.,0.,1.92296268638356E-16));
#10604=DIRECTION('',(-1.,0.,-1.92296268638356E-16));
#10605=DIRECTION('',(0.,-1.,0.));
#10606=DIRECTION('',(1.,0.,1.92296268638356E-16));
#10607=DIRECTION('center_axis',(-0.866025403784439,0.,-0.5));
#10608=DIRECTION('ref_axis',(0.5,0.,-0.866025403784439));
#10609=DIRECTION('',(-0.5,0.,0.866025403784438));
#10610=DIRECTION('',(0.,-1.,0.));
#10611=DIRECTION('',(0.5,0.,-0.866025403784438));
#10612=DIRECTION('center_axis',(-0.866025403784439,0.,0.5));
#10613=DIRECTION('ref_axis',(-0.5,0.,-0.866025403784439));
#10614=DIRECTION('',(0.5,0.,0.866025403784439));
#10615=DIRECTION('',(0.,-1.,0.));
#10616=DIRECTION('',(-0.5,0.,-0.866025403784439));
#10617=DIRECTION('center_axis',(-1.92296268638356E-16,0.,1.));
#10618=DIRECTION('ref_axis',(-1.,0.,-1.92296268638356E-16));
#10619=DIRECTION('',(1.,0.,1.92296268638356E-16));
#10620=DIRECTION('',(0.,-1.,0.));
#10621=DIRECTION('',(-1.,0.,-1.92296268638356E-16));
#10622=DIRECTION('center_axis',(0.866025403784439,0.,0.5));
#10623=DIRECTION('ref_axis',(-0.5,0.,0.866025403784439));
#10624=DIRECTION('',(0.5,0.,-0.866025403784439));
#10625=DIRECTION('',(-0.5,0.,0.866025403784439));
#10626=DIRECTION('center_axis',(0.,1.,0.));
#10627=DIRECTION('ref_axis',(1.,0.,0.));
#10628=DIRECTION('center_axis',(0.,-1.,0.));
#10629=DIRECTION('ref_axis',(0.,0.,-1.));
#10630=DIRECTION('center_axis',(0.,1.,0.));
#10631=DIRECTION('ref_axis',(1.,0.,0.));
#10632=DIRECTION('center_axis',(0.,1.,0.));
#10633=DIRECTION('ref_axis',(1.,0.,0.));
#10634=DIRECTION('center_axis',(0.,1.,0.));
#10635=DIRECTION('ref_axis',(0.,0.,1.));
#10636=DIRECTION('center_axis',(0.,-1.,0.));
#10637=DIRECTION('ref_axis',(1.,0.,0.));
#10638=DIRECTION('center_axis',(0.,-1.,0.));
#10639=DIRECTION('ref_axis',(1.,0.,0.));
#10640=DIRECTION('center_axis',(0.,-1.,0.));
#10641=DIRECTION('ref_axis',(1.,0.,0.));
#10642=DIRECTION('',(0.707106781186548,0.707106781186547,8.65956056235494E-17));
#10643=DIRECTION('center_axis',(0.,-1.,0.));
#10644=DIRECTION('ref_axis',(1.,0.,0.));
#10645=DIRECTION('center_axis',(0.,-1.,0.));
#10646=DIRECTION('ref_axis',(1.,0.,0.));
#10647=DIRECTION('',(0.,1.,0.));
#10648=DIRECTION('center_axis',(0.,1.,0.));
#10649=DIRECTION('ref_axis',(1.,0.,0.));
#10650=DIRECTION('center_axis',(0.,-1.,0.));
#10651=DIRECTION('ref_axis',(1.,0.,0.));
#10652=DIRECTION('',(-0.707106781186547,0.707106781186548,-8.65956056235493E-17));
#10653=DIRECTION('center_axis',(0.,-1.,0.));
#10654=DIRECTION('ref_axis',(0.,0.,-1.));
#10655=DIRECTION('center_axis',(0.,-1.,0.));
#10656=DIRECTION('ref_axis',(1.,0.,0.));
#10657=DIRECTION('center_axis',(0.,1.,0.));
#10658=DIRECTION('ref_axis',(1.,0.,0.));
#10659=DIRECTION('center_axis',(0.,1.,0.));
#10660=DIRECTION('ref_axis',(1.,0.,0.));
#10661=DIRECTION('',(-0.447213595499958,0.894427190999916,-5.47678698264203E-17));
#10662=DIRECTION('center_axis',(0.,-1.,0.));
#10663=DIRECTION('ref_axis',(1.,0.,0.));
#10664=DIRECTION('',(0.,1.,0.));
#13330=CARTESIAN_POINT('',(0.,0.,0.));
#13331=CARTESIAN_POINT('Origin',(0.144337567297406,-0.6,-0.25));
#13332=CARTESIAN_POINT('',(0.288675134594813,-0.6,0.));
#13333=CARTESIAN_POINT('',(0.144337567297406,-0.6,-0.25));
#13334=CARTESIAN_POINT('',(0.288675134594813,-0.6,0.));
#13335=CARTESIAN_POINT('',(0.144337567297406,-0.96,-0.25));
#13336=CARTESIAN_POINT('',(0.144337567297406,-0.6,-0.25));
#13337=CARTESIAN_POINT('',(0.288675134594813,-0.96,0.));
#13338=CARTESIAN_POINT('',(0.288675134594813,-0.96,0.));
#13339=CARTESIAN_POINT('',(0.288675134594813,-0.6,0.));
#13340=CARTESIAN_POINT('Origin',(-0.144337567297406,-0.6,-0.25));
#13341=CARTESIAN_POINT('',(-0.144337567297406,-0.6,-0.25));
#13342=CARTESIAN_POINT('',(0.144337567297406,-0.6,-0.25));
#13343=CARTESIAN_POINT('',(-0.144337567297406,-0.96,-0.25));
#13344=CARTESIAN_POINT('',(-0.144337567297406,-0.6,-0.25));
#13345=CARTESIAN_POINT('',(0.144337567297406,-0.96,-0.25));
#13346=CARTESIAN_POINT('Origin',(-0.288675134594813,-0.6,-8.32667268468867E-17));
#13347=CARTESIAN_POINT('',(-0.288675134594813,-0.6,-3.53525079574969E-17));
#13348=CARTESIAN_POINT('',(-0.144337567297406,-0.6,-0.25));
#13349=CARTESIAN_POINT('',(-0.288675134594813,-0.96,-5.55111512312578E-17));
#13350=CARTESIAN_POINT('',(-0.288675134594813,-0.6,-3.53525079574969E-17));
#13351=CARTESIAN_POINT('',(-0.144337567297406,-0.96,-0.25));
#13352=CARTESIAN_POINT('Origin',(-0.144337567297407,-0.6,0.25));
#13353=CARTESIAN_POINT('',(-0.144337567297407,-0.6,0.25));
#13354=CARTESIAN_POINT('',(-0.288675134594813,-0.6,-3.53525079574969E-17));
#13355=CARTESIAN_POINT('',(-0.144337567297407,-0.96,0.25));
#13356=CARTESIAN_POINT('',(-0.144337567297407,-0.6,0.25));
#13357=CARTESIAN_POINT('',(-0.288675134594813,-0.96,-3.53525079574969E-17));
#13358=CARTESIAN_POINT('Origin',(0.144337567297406,-0.6,0.25));
#13359=CARTESIAN_POINT('',(0.144337567297406,-0.6,0.25));
#13360=CARTESIAN_POINT('',(-0.144337567297407,-0.6,0.25));
#13361=CARTESIAN_POINT('',(0.144337567297406,-0.96,0.25));
#13362=CARTESIAN_POINT('',(0.144337567297406,-0.6,0.25));
#13363=CARTESIAN_POINT('',(-0.144337567297407,-0.96,0.25));
#13364=CARTESIAN_POINT('Origin',(0.288675134594813,-0.6,0.));
#13365=CARTESIAN_POINT('',(0.144337567297406,-0.6,0.25));
#13366=CARTESIAN_POINT('',(0.144337567297406,-0.96,0.25));
#13367=CARTESIAN_POINT('Origin',(0.,-0.6,0.));
#13368=CARTESIAN_POINT('Origin',(0.,-0.96,0.));
#13369=CARTESIAN_POINT('Origin',(0.,-1.8,0.));
#13370=CARTESIAN_POINT('',(-0.2942,-1.8,3.60291088309151E-17));
#13371=CARTESIAN_POINT('Origin',(0.,-1.8,0.));
#13372=CARTESIAN_POINT('Origin',(0.45,0.6,0.));
#13373=CARTESIAN_POINT('',(-0.45,0.6,-5.51091059616309E-17));
#13374=CARTESIAN_POINT('Origin',(0.,0.6,0.));
#13375=CARTESIAN_POINT('Origin',(0.,0.575,0.));
#13376=CARTESIAN_POINT('',(-0.5,0.55,-6.12323399573677E-17));
#13377=CARTESIAN_POINT('Origin',(0.,0.55,0.));
#13378=CARTESIAN_POINT('',(-0.475,0.575,-5.81707229594993E-17));
#13379=CARTESIAN_POINT('Origin',(0.,0.29,0.));
#13380=CARTESIAN_POINT('',(-0.5,0.0299999999999998,-6.12323399573677E-17));
#13381=CARTESIAN_POINT('Origin',(0.,0.0299999999999998,0.));
#13382=CARTESIAN_POINT('',(-0.5,0.29,-6.12323399573677E-17));
#13383=CARTESIAN_POINT('Origin',(0.,0.0150000000000001,0.));
#13384=CARTESIAN_POINT('',(-0.47,7.11236625150491E-17,-5.75583995599256E-17));
#13385=CARTESIAN_POINT('Origin',(0.,0.,0.));
#13386=CARTESIAN_POINT('',(-0.485,0.0150000000000001,-5.93953697586466E-17));
#13387=CARTESIAN_POINT('Origin',(0.32,0.,0.));
#13388=CARTESIAN_POINT('',(-0.32,-6.93889390390723E-18,-3.91886975727153E-17));
#13389=CARTESIAN_POINT('Origin',(0.,0.,0.));
#13390=CARTESIAN_POINT('Origin',(0.,-0.02,0.));
#13391=CARTESIAN_POINT('',(-0.2942,-0.0515999999999999,3.60291088309151E-17));
#13392=CARTESIAN_POINT('Origin',(0.,-0.0515999999999999,0.));
#13393=CARTESIAN_POINT('',(-0.31,-0.02,-3.7964050773568E-17));
#13394=CARTESIAN_POINT('Origin',(0.,-1.24,0.));
#13395=CARTESIAN_POINT('',(-0.2942,-1.24,-3.60291088309151E-17));
#16149=UNCERTAINTY_MEASURE_WITH_UNIT(LENGTH_MEASURE(0.001),#16282,
'DISTANCE_ACCURACY_VALUE',
'Maximum model space distance between geometric entities at asserted c
onnectivities');
#16212=UNCERTAINTY_MEASURE_WITH_UNIT(LENGTH_MEASURE(0.001),#16282,
'DISTANCE_ACCURACY_VALUE',
'Maximum model space distance between geometric entities at asserted c
onnectivities');
#16218=(
GEOMETRIC_REPRESENTATION_CONTEXT(3)
GLOBAL_UNCERTAINTY_ASSIGNED_CONTEXT((#16149))
GLOBAL_UNIT_ASSIGNED_CONTEXT((#16282,#16284,#16285))
REPRESENTATION_CONTEXT('','3D')
);
#16281=(
GEOMETRIC_REPRESENTATION_CONTEXT(3)
GLOBAL_UNCERTAINTY_ASSIGNED_CONTEXT((#16212))
GLOBAL_UNIT_ASSIGNED_CONTEXT((#16282,#16284,#16285))
REPRESENTATION_CONTEXT('','3D')
);
#16282=(
LENGTH_UNIT()
NAMED_UNIT(*)
SI_UNIT(.CENTI.,.METRE.)
);
#16284=(
NAMED_UNIT(*)
PLANE_ANGLE_UNIT()
SI_UNIT($,.RADIAN.)
);
#16285=(
NAMED_UNIT(*)
SI_UNIT($,.STERADIAN.)
SOLID_ANGLE_UNIT()
);
#16291=SHAPE_DEFINITION_REPRESENTATION(#16359,#16524);
#16359=PRODUCT_DEFINITION_SHAPE('',$,#16593);
#16524=SHAPE_REPRESENTATION('',(#9206),#16218);
#16587=PRODUCT_DEFINITION_CONTEXT('part definition',#16793,'design');
#16593=PRODUCT_DEFINITION('M6x18 mounting screw','M6x18 mounting screw',
#16661,#16587);
#16661=PRODUCT_DEFINITION_FORMATION('',$,#16800);
#16793=APPLICATION_CONTEXT(
'Core Data for Automotive Mechanical Design Process');
#16794=PRODUCT_CONTEXT('part definition',#16793,'mechanical');
#16800=PRODUCT('M6x18 mounting screw','M6x18 mounting screw',
'M6x18 mounting screw',(#16794));
#16933=COLOUR_RGB('Black',0.12,0.14,0.17);
#16934=FILL_AREA_STYLE_COLOUR('',#16933);
#16935=FILL_AREA_STYLE('',(#16934));
#16936=SURFACE_STYLE_FILL_AREA(#16935);
#16937=SURFACE_SIDE_STYLE('',(#16936));
#16938=SURFACE_STYLE_USAGE(.BOTH.,#16937);
#16939=PRESENTATION_STYLE_ASSIGNMENT((#16938));
ENDSEC;
END-ISO-10303-21;
